ISO-10303-21;
HEADER;
FILE_DESCRIPTION (('STEP AP214'),
    '1' );
FILE_NAME ('Tip.step',
    '2026-10-06T14:00:01',
    ( '' ),
    ( '' ),
    'SwSTEP 2.0',
    'SolidWorks 2020',
    '' );
FILE_SCHEMA (( 'AUTOMOTIVE_DESIGN' ));
ENDSEC;

DATA;
#95=DIRECTION ( 'NONE',  ( 0.000000000000000000, -0.9996898646859343485, -0.02490330187381123786 ) ) ;
#265=FILL_AREA_STYLE_COLOUR ( '', #10390 ) ;
#273=EDGE_LOOP ( 'NONE', ( #11335, #9422, #18646, #936 ) ) ;
#296=( GEOMETRIC_REPRESENTATION_CONTEXT ( 3 ) GLOBAL_UNCERTAINTY_ASSIGNED_CONTEXT ( ( #20279 ) ) GLOBAL_UNIT_ASSIGNED_CONTEXT ( ( #24942, #22905, #24798 ) ) REPRESENTATION_CONTEXT ( 'NONE', 'WORKASPACE' ) );
#313=PRODUCT_DEFINITION_CONTEXT ( 'detailed design', #27985, 'design' ) ;
#317=DIRECTION ( 'NONE',  ( 1.000000000000000000, 3.053848253006669023E-16, -2.042510438544995415E-16 ) ) ;
#337=ORIENTED_EDGE ( 'NONE', *, *, #17482, .F. ) ;
#355=VERTEX_POINT ( 'NONE', #14878 ) ;
#498=CARTESIAN_POINT ( 'NONE',  ( -77.28999999999996362, -3.470778894058966809E-15, 5.300300110251643219E-15 ) ) ;
#630=LINE ( 'NONE', #9997, #12984 ) ;
#936=ORIENTED_EDGE ( 'NONE', *, *, #23568, .F. ) ;
#1206=FACE_BOUND ( 'NONE', #14694, .T. ) ;
#1243=EDGE_LOOP ( 'NONE', ( #30408, #28047, #15789, #9686 ) ) ;
#1244=EDGE_LOOP ( 'NONE', ( #29227, #20470, #20678, #22948 ) ) ;
#1246=PLANE ( 'NONE',  #19210 ) ;
#1513=CARTESIAN_POINT ( 'NONE',  ( -77.28999999999996362, -0.2599193648183464878, -0.006474858487185624310 ) ) ;
#1695=DIRECTION ( 'NONE',  ( 1.000000000000000000, 3.053848253006669023E-16, -2.042510438544995415E-16 ) ) ;
#1850=AXIS2_PLACEMENT_3D ( 'NONE', #6631, #30519, #23420 ) ;
#1925=CIRCLE ( 'NONE', #26709, 0.01000000000000001929 ) ;
#1936=( NAMED_UNIT ( * ) PLANE_ANGLE_UNIT ( ) SI_UNIT ( $, .RADIAN. ) );
#2211=AXIS2_PLACEMENT_3D ( 'NONE', #28907, #7217, #95 ) ;
#2282=CARTESIAN_POINT ( 'NONE',  ( -77.29999999999998295, -3.473832742311974792E-15, 5.302342620690189014E-15 ) ) ;
#2445=EDGE_CURVE ( 'NONE', #20300, #355, #10467, .T. ) ;
#2957=AXIS2_PLACEMENT_3D ( 'NONE', #19950, #27379, #27855 ) ;
#2963=CARTESIAN_POINT ( 'NONE',  ( -77.28999999999996362, -0.4498604391086740151, -0.01120648584320975590 ) ) ;
#3121=CARTESIAN_POINT ( 'NONE',  ( -77.29999999999998295, 0.2599193648183395489, 0.006474858487196258165 ) ) ;
#3129=CARTESIAN_POINT ( 'NONE',  ( -77.28999999999996362, 0.4398635404618077005, 0.01095745282448230135 ) ) ;
#3235=ORIENTED_EDGE ( 'NONE', *, *, #30579, .F. ) ;
#3299=VECTOR ( 'NONE', #11724, 1000.000000000000000 ) ;
#3312=CYLINDRICAL_SURFACE ( 'NONE', #2957, 0.4500000000000001221 ) ;
#3372=CIRCLE ( 'NONE', #19641, 0.4500000000000001221 ) ;
#3463=FACE_OUTER_BOUND ( 'NONE', #23795, .T. ) ;
#3540=TOROIDAL_SURFACE ( 'NONE', #21756, 0.2600000000000000089, 0.01000000000000000021 ) ;
#3735=DIRECTION ( 'NONE',  ( -1.000000000000000000, -3.053848253006669023E-16, 2.042510438544995169E-16 ) ) ;
#3740=EDGE_CURVE ( 'NONE', #9407, #8968, #3755, .T. ) ;
#3755=CIRCLE ( 'NONE', #12825, 0.4400000000000000577 ) ;
#3768=VERTEX_POINT ( 'NONE', #2963 ) ;
#3796=DIRECTION ( 'NONE',  ( 0.000000000000000000, -0.9996898646859343485, -0.02490330187381123786 ) ) ;
#3860=CARTESIAN_POINT ( 'NONE',  ( -77.28999999999996362, -3.470778894058966809E-15, 5.300300110251643219E-15 ) ) ;
#4050=DIRECTION ( 'NONE',  ( 0.000000000000000000, -0.9996898646859343485, -0.02490330187381123786 ) ) ;
#4133=CARTESIAN_POINT ( 'NONE',  ( -77.28999999999996362, -0.4398635404618146394, -0.01095745282447164494 ) ) ;
#4177=AXIS2_PLACEMENT_3D ( 'NONE', #4133, #26874, #19622 ) ;
#4254=SHAPE_DEFINITION_REPRESENTATION ( #29783, #16755 ) ;
#4400=ORIENTED_EDGE ( 'NONE', *, *, #8203, .F. ) ;
#4437=CARTESIAN_POINT ( 'NONE',  ( -77.28999999999996362, -3.470778894058966809E-15, 5.300300110251643219E-15 ) ) ;
#4464=PRESENTATION_STYLE_ASSIGNMENT (( #6529 ) ) ;
#4475=COLOUR_RGB ( '', 0.72549020, 0.75294118, 0.79215686) ;
#4547=ADVANCED_FACE ( 'NONE', ( #15814 ), #3312, .T. ) ;
#4609=FACE_OUTER_BOUND ( 'NONE', #29544, .T. ) ;
#4700=FILL_AREA_STYLE ('',( #265 ) ) ;
#4844=VERTEX_POINT ( 'NONE', #3121 ) ;
#4898=AXIS2_PLACEMENT_3D ( 'NONE', #6398, #21575, #11143 ) ;
#4980=CARTESIAN_POINT ( 'NONE',  ( -77.29999999999998295, -0.2599193648183464878, -0.006474858487185622576 ) ) ;
#5357=ADVANCED_FACE ( 'NONE', ( #6027, #30061 ), #1246, .F. ) ;
#5648=CARTESIAN_POINT ( 'NONE',  ( -77.29999999999998295, -3.473832742311974792E-15, 5.302342620690189014E-15 ) ) ;
#5748=EDGE_CURVE ( 'NONE', #23038, #26062, #22131, .T. ) ;
#5955=EDGE_CURVE ( 'NONE', #18823, #9407, #16568, .T. ) ;
#6027=FACE_BOUND ( 'NONE', #23999, .T. ) ;
#6040=PRODUCT_DEFINITION ( 'UNKNOWN', '', #15160, #313 ) ;
#6054=CARTESIAN_POINT ( 'NONE',  ( -77.28999999999996362, -3.470778894058966809E-15, 5.300300110251643219E-15 ) ) ;
#6304=FACE_OUTER_BOUND ( 'NONE', #18155, .T. ) ;
#6398=CARTESIAN_POINT ( 'NONE',  ( -44.49999999999997868, 6.542789527549899840E-15, -1.397091617737396343E-15 ) ) ;
#6413=ORIENTED_EDGE ( 'NONE', *, *, #26831, .T. ) ;
#6529=SURFACE_STYLE_USAGE ( .BOTH. , #28526 ) ;
#6555=ORIENTED_EDGE ( 'NONE', *, *, #3740, .T. ) ;
#6631=CARTESIAN_POINT ( 'NONE',  ( -77.29999999999998295, -3.473832742311974792E-15, 5.302342620690189014E-15 ) ) ;
#6787=ADVANCED_FACE ( 'NONE', ( #3463 ), #3540, .T. ) ;
#7011=ORIENTED_EDGE ( 'NONE', *, *, #3740, .F. ) ;
#7096=FACE_OUTER_BOUND ( 'NONE', #1243, .T. ) ;
#7098=SURFACE_STYLE_USAGE ( .BOTH. , #9931 ) ;
#7119=ORIENTED_EDGE ( 'NONE', *, *, #12535, .F. ) ;
#7217=DIRECTION ( 'NONE',  ( 1.000000000000000000, 3.053848253006669023E-16, -2.042510438544995415E-16 ) ) ;
#7378=ORIENTED_EDGE ( 'NONE', *, *, #7735, .T. ) ;
#7735=EDGE_CURVE ( 'NONE', #4844, #8781, #11677, .T. ) ;
#7924=SHAPE_REPRESENTATION_RELATIONSHIP ( 'NONE' , 'NONE' ,  #16755, #27821 ) ;
#7995=VERTEX_POINT ( 'NONE', #25143 ) ;
#8054=PRODUCT ( 'Tip', 'Tip', '', ( #13898 ) ) ;
#8070=FACE_OUTER_BOUND ( 'NONE', #30748, .T. ) ;
#8203=EDGE_CURVE ( 'NONE', #26062, #23038, #30918, .T. ) ;
#8348=CARTESIAN_POINT ( 'NONE',  ( -77.28999999999996362, -3.470778894058966809E-15, 5.300300110251643219E-15 ) ) ;
#8367=DIRECTION ( 'NONE',  ( -1.000000000000000000, -3.053848253006669023E-16, 2.042510438544995415E-16 ) ) ;
#8516=DIRECTION ( 'NONE',  ( 0.000000000000000000, -0.9996898646859343485, -0.02490330187381123786 ) ) ;
#8646=DIRECTION ( 'NONE',  ( 3.002035892788116966E-16, -0.9996898646859343485, -0.02490330187381123786 ) ) ;
#8661=DIRECTION ( 'NONE',  ( -1.000000000000000000, -3.053848253006669023E-16, 2.042510438544995415E-16 ) ) ;
#8668=EDGE_CURVE ( 'NONE', #8968, #9407, #10206, .T. ) ;
#8682=AXIS2_PLACEMENT_3D ( 'NONE', #2282, #11948, #28742 ) ;
#8781=VERTEX_POINT ( 'NONE', #4980 ) ;
#8947=AXIS2_PLACEMENT_3D ( 'NONE', #498, #11799, #24555 ) ;
#8968=VERTEX_POINT ( 'NONE', #16312 ) ;
#9018=AXIS2_PLACEMENT_3D ( 'NONE', #25987, #9060, #11596 ) ;
#9060=DIRECTION ( 'NONE',  ( 0.000000000000000000, 0.000000000000000000, 1.000000000000000000 ) ) ;
#9175=ORIENTED_EDGE ( 'NONE', *, *, #28628, .T. ) ;
#9223=( NAMED_UNIT ( * ) SI_UNIT ( $, .STERADIAN. ) SOLID_ANGLE_UNIT ( ) );
#9272=DIRECTION ( 'NONE',  ( -1.000000000000000000, -3.053848253006669023E-16, 2.042510438544995415E-16 ) ) ;
#9407=VERTEX_POINT ( 'NONE', #27444 ) ;
#9422=ORIENTED_EDGE ( 'NONE', *, *, #5955, .T. ) ;
#9501=AXIS2_PLACEMENT_3D ( 'NONE', #3129, #20719, #15162 ) ;
#9672=LINE ( 'NONE', #31191, #10906 ) ;
#9686=ORIENTED_EDGE ( 'NONE', *, *, #17336, .T. ) ;
#9931=SURFACE_SIDE_STYLE ('',( #28784 ) ) ;
#9997=CARTESIAN_POINT ( 'NONE',  ( -77.29999999999998295, 0.4498604391086670762, 0.01120648584322036373 ) ) ;
#10108=DIRECTION ( 'NONE',  ( 0.000000000000000000, -0.9996898646859344595, -0.02490330187381131419 ) ) ;
#10206=CIRCLE ( 'NONE', #8682, 0.4400000000000000577 ) ;
#10255=DIRECTION ( 'NONE',  ( 2.117927888850091331E-16, -0.02490330187381135929, 0.9996898646859343485 ) ) ;
#10390=COLOUR_RGB ( '', 0.72549020, 0.75294118, 0.79215686) ;
#10451=CARTESIAN_POINT ( 'NONE',  ( -73.89999999999997726, -2.435524336289708093E-15, 4.607889071584891164E-15 ) ) ;
#10467=LINE ( 'NONE', #27081, #27804 ) ;
#10677=ORIENTED_EDGE ( 'NONE', *, *, #16600, .F. ) ;
#10906=VECTOR ( 'NONE', #26589, 1000.000000000000000 ) ;
#10993=CIRCLE ( 'NONE', #28704, 0.4500000000000001221 ) ;
#11141=DIRECTION ( 'NONE',  ( 3.002035892788117952E-16, -0.9996898646859344595, -0.02490330187381124480 ) ) ;
#11143=DIRECTION ( 'NONE',  ( 0.000000000000000000, -0.9996898646859343485, -0.02490330187381123786 ) ) ;
#11171=DIRECTION ( 'NONE',  ( -2.117927888850090838E-16, 0.02490330187381123786, -0.9996898646859343485 ) ) ;
#11335=ORIENTED_EDGE ( 'NONE', *, *, #29349, .F. ) ;
#11596=DIRECTION ( 'NONE',  ( 1.000000000000000000, 0.000000000000000000, 0.000000000000000000 ) ) ;
#11646=CARTESIAN_POINT ( 'NONE',  ( -77.28999999999996362, -3.470778894058966809E-15, 5.300300110251643219E-15 ) ) ;
#11677=CIRCLE ( 'NONE', #23314, 0.2600000000000000644 ) ;
#11724=DIRECTION ( 'NONE',  ( 1.000000000000000000, 3.053848253006669023E-16, -2.042510438544995415E-16 ) ) ;
#11799=DIRECTION ( 'NONE',  ( -1.000000000000000000, -3.053848253006669023E-16, 2.042510438544995415E-16 ) ) ;
#11834=DIRECTION ( 'NONE',  ( 0.000000000000000000, -0.9996898646859343485, -0.02490330187381123786 ) ) ;
#11948=DIRECTION ( 'NONE',  ( -1.000000000000000000, -3.053848253006669023E-16, 2.042510438544995415E-16 ) ) ;
#12052=UNCERTAINTY_MEASURE_WITH_UNIT (LENGTH_MEASURE( 1.000000000000000082E-05 ), #25837, 'distance_accuracy_value', 'NONE');
#12426=ADVANCED_FACE ( 'NONE', ( #4609 ), #26458, .F. ) ;
#12535=EDGE_CURVE ( 'NONE', #18823, #26062, #630, .T. ) ;
#12621=DIRECTION ( 'NONE',  ( 0.000000000000000000, -0.9996898646859343485, -0.02490330187381123786 ) ) ;
#12825=AXIS2_PLACEMENT_3D ( 'NONE', #5648, #17533, #18281 ) ;
#12984=VECTOR ( 'NONE', #27237, 1000.000000000000000 ) ;
#13363=FACE_OUTER_BOUND ( 'NONE', #273, .T. ) ;
#13367=DIRECTION ( 'NONE',  ( 1.000000000000000000, 3.053848253006669023E-16, -2.042510438544995415E-16 ) ) ;
#13404=ORIENTED_EDGE ( 'NONE', *, *, #18377, .T. ) ;
#13416=CIRCLE ( 'NONE', #19549, 0.2500000000000000555 ) ;
#13437=DIRECTION ( 'NONE',  ( -1.000000000000000000, -3.053848253006669023E-16, 2.042510438544995415E-16 ) ) ;
#13455=DIRECTION ( 'NONE',  ( 0.000000000000000000, -0.9996898646859343485, -0.02490330187381123786 ) ) ;
#13569=( GEOMETRIC_REPRESENTATION_CONTEXT ( 3 ) GLOBAL_UNCERTAINTY_ASSIGNED_CONTEXT ( ( #12052 ) ) GLOBAL_UNIT_ASSIGNED_CONTEXT ( ( #25837, #26316, #28849 ) ) REPRESENTATION_CONTEXT ( 'NONE', 'WORKASPACE' ) );
#13692=CARTESIAN_POINT ( 'NONE',  ( -77.28999999999996362, -3.470778894058966809E-15, 5.300300110251643219E-15 ) ) ;
#13898=PRODUCT_CONTEXT ( 'NONE', #26924, 'mechanical' ) ;
#13901=DIRECTION ( 'NONE',  ( 1.000000000000000000, 3.053848253006669023E-16, -2.042510438544995415E-16 ) ) ;
#14025=AXIS2_PLACEMENT_3D ( 'NONE', #30990, #30678, #11834 ) ;
#14310=TOROIDAL_SURFACE ( 'NONE', #24413, 0.4399999999999999467, 0.01000000000000000021 ) ;
#14327=TOROIDAL_SURFACE ( 'NONE', #23442, 0.2600000000000000089, 0.01000000000000000021 ) ;
#14372=CARTESIAN_POINT ( 'NONE',  ( -73.89999999999997726, -2.435524336289708093E-15, 4.607889071584891164E-15 ) ) ;
#14407=DIRECTION ( 'NONE',  ( 0.000000000000000000, -0.9996898646859343485, -0.02490330187381123786 ) ) ;
#14434=ADVANCED_FACE ( 'NONE', ( #13363 ), #20016, .T. ) ;
#14529=ORIENTED_EDGE ( 'NONE', *, *, #5748, .T. ) ;
#14545=DIRECTION ( 'NONE',  ( -1.000000000000000000, -3.053848253006669023E-16, 2.042510438544995415E-16 ) ) ;
#14694=EDGE_LOOP ( 'NONE', ( #25908, #7378 ) ) ;
#14878=CARTESIAN_POINT ( 'NONE',  ( -77.28999999999996362, 0.2499224661714801732, 0.006225825468458142005 ) ) ;
#14901=ORIENTED_EDGE ( 'NONE', *, *, #30579, .T. ) ;
#14942=ORIENTED_EDGE ( 'NONE', *, *, #7735, .F. ) ;
#15019=AXIS2_PLACEMENT_3D ( 'NONE', #25433, #3735, #8646 ) ;
#15127=MANIFOLD_SOLID_BREP ( 'Stock-MAS-683-1', #22632 ) ;
#15160=PRODUCT_DEFINITION_FORMATION_WITH_SPECIFIED_SOURCE ( 'ANY', '', #8054, .NOT_KNOWN. ) ;
#15162=DIRECTION ( 'NONE',  ( 0.000000000000000000, -0.9996898646859344595, -0.02490330187381139398 ) ) ;
#15500=CIRCLE ( 'NONE', #1850, 0.2600000000000000644 ) ;
#15649=DIRECTION ( 'NONE',  ( 3.002035892788117459E-16, -0.9996898646859343485, -0.02490330187381124133 ) ) ;
#15789=ORIENTED_EDGE ( 'NONE', *, *, #17482, .T. ) ;
#15814=FACE_OUTER_BOUND ( 'NONE', #1244, .T. ) ;
#15819=DIRECTION ( 'NONE',  ( -1.000000000000000000, -3.053848253006669023E-16, 2.042510438544995169E-16 ) ) ;
#16279=CYLINDRICAL_SURFACE ( 'NONE', #14025, 0.2500000000000000555 ) ;
#16312=CARTESIAN_POINT ( 'NONE',  ( -77.29999999999998295, -0.4398635404618146394, -0.01095745282447164320 ) ) ;
#16501=( LENGTH_UNIT ( ) NAMED_UNIT ( * ) SI_UNIT ( .MILLI., .METRE. ) );
#16568=CIRCLE ( 'NONE', #9501, 0.01000000000000001929 ) ;
#16600=EDGE_CURVE ( 'NONE', #355, #28086, #17981, .T. ) ;
#16755=SHAPE_REPRESENTATION ( 'Tip', ( #9018 ), #18147 ) ;
#16758=PRESENTATION_STYLE_ASSIGNMENT (( #7098 ) ) ;
#17096=AXIS2_PLACEMENT_3D ( 'NONE', #1513, #11171, #18469 ) ;
#17309=EDGE_LOOP ( 'NONE', ( #31203, #6555 ) ) ;
#17336=EDGE_CURVE ( 'NONE', #28086, #355, #13416, .T. ) ;
#17482=EDGE_CURVE ( 'NONE', #7995, #28086, #9672, .T. ) ;
#17533=DIRECTION ( 'NONE',  ( -1.000000000000000000, -3.053848253006669023E-16, 2.042510438544995415E-16 ) ) ;
#17981=CIRCLE ( 'NONE', #22037, 0.2500000000000000555 ) ;
#18147=( GEOMETRIC_REPRESENTATION_CONTEXT ( 3 ) GLOBAL_UNCERTAINTY_ASSIGNED_CONTEXT ( ( #30053 ) ) GLOBAL_UNIT_ASSIGNED_CONTEXT ( ( #16501, #1936, #9223 ) ) REPRESENTATION_CONTEXT ( 'NONE', 'WORKASPACE' ) );
#18155=EDGE_LOOP ( 'NONE', ( #28918, #13404, #14529, #7119 ) ) ;
#18175=ORIENTED_EDGE ( 'NONE', *, *, #2445, .T. ) ;
#18182=FACE_OUTER_BOUND ( 'NONE', #17309, .T. ) ;
#18281=DIRECTION ( 'NONE',  ( 0.000000000000000000, -0.9996898646859344595, -0.02490330187381123786 ) ) ;
#18377=EDGE_CURVE ( 'NONE', #3768, #23038, #25655, .T. ) ;
#18469=DIRECTION ( 'NONE',  ( 0.000000000000000000, 0.9996898646859344595, 0.02490330187381122745 ) ) ;
#18574=ORIENTED_EDGE ( 'NONE', *, *, #16600, .T. ) ;
#18621=CIRCLE ( 'NONE', #31244, 0.2500000000000000555 ) ;
#18646=ORIENTED_EDGE ( 'NONE', *, *, #8668, .F. ) ;
#18767=EDGE_LOOP ( 'NONE', ( #4400, #24691 ) ) ;
#18822=CARTESIAN_POINT ( 'NONE',  ( -77.28999999999996362, 0.4498604391086670762, 0.01120648584322041577 ) ) ;
#18823=VERTEX_POINT ( 'NONE', #18822 ) ;
#18882=FILL_AREA_STYLE_COLOUR ( '', #4475 ) ;
#19210=AXIS2_PLACEMENT_3D ( 'NONE', #10451, #15819, #23123 ) ;
#19399=ORIENTED_EDGE ( 'NONE', *, *, #26831, .F. ) ;
#19549=AXIS2_PLACEMENT_3D ( 'NONE', #4437, #13437, #3796 ) ;
#19622=DIRECTION ( 'NONE',  ( 0.000000000000000000, 0.9996898646859344595, 0.02490330187381122745 ) ) ;
#19641=AXIS2_PLACEMENT_3D ( 'NONE', #6054, #27884, #13455 ) ;
#19657=CARTESIAN_POINT ( 'NONE',  ( -73.89999999999997726, -2.435524336289708093E-15, 4.607889071584891164E-15 ) ) ;
#19950=CARTESIAN_POINT ( 'NONE',  ( -77.29999999999998295, -3.473832742311974792E-15, 5.302342620690189014E-15 ) ) ;
#20016=TOROIDAL_SURFACE ( 'NONE', #8947, 0.4399999999999999467, 0.01000000000000000021 ) ;
#20094=CARTESIAN_POINT ( 'NONE',  ( -77.28999999999996362, 0.2599193648183395489, 0.006474858487196256430 ) ) ;
#20279=UNCERTAINTY_MEASURE_WITH_UNIT (LENGTH_MEASURE( 1.000000000000000082E-05 ), #24942, 'distance_accuracy_value', 'NONE');
#20300=VERTEX_POINT ( 'NONE', #22219 ) ;
#20427=CARTESIAN_POINT ( 'NONE',  ( -77.28999999999996362, -3.470778894058966809E-15, 5.300300110251643219E-15 ) ) ;
#20470=ORIENTED_EDGE ( 'NONE', *, *, #26720, .T. ) ;
#20554=PLANE ( 'NONE',  #15019 ) ;
#20673=DIRECTION ( 'NONE',  ( -1.000000000000000000, -3.053848253006669023E-16, 2.042510438544995415E-16 ) ) ;
#20678=ORIENTED_EDGE ( 'NONE', *, *, #12535, .T. ) ;
#20714=ORIENTED_EDGE ( 'NONE', *, *, #5955, .F. ) ;
#20719=DIRECTION ( 'NONE',  ( 2.117927888850091331E-16, -0.02490330187381135929, 0.9996898646859343485 ) ) ;
#20763=ADVANCED_FACE ( 'NONE', ( #8070 ), #14327, .T. ) ;
#20942=SURFACE_STYLE_FILL_AREA ( #21584 ) ;
#21290=EDGE_CURVE ( 'NONE', #20300, #7995, #27480, .T. ) ;
#21319=ORIENTED_EDGE ( 'NONE', *, *, #21290, .F. ) ;
#21567=STYLED_ITEM ( 'NONE', ( #16758 ), #15127 ) ;
#21575=DIRECTION ( 'NONE',  ( -1.000000000000000000, -3.053848253006669023E-16, 2.042510438544995415E-16 ) ) ;
#21584=FILL_AREA_STYLE ('',( #18882 ) ) ;
#21756=AXIS2_PLACEMENT_3D ( 'NONE', #8348, #30662, #15649 ) ;
#21932=ORIENTED_EDGE ( 'NONE', *, *, #17336, .F. ) ;
#22037=AXIS2_PLACEMENT_3D ( 'NONE', #11646, #9272, #30798 ) ;
#22131=CIRCLE ( 'NONE', #23642, 0.4500000000000001221 ) ;
#22192=STYLED_ITEM ( 'NONE', ( #4464 ), #27821 ) ;
#22219=CARTESIAN_POINT ( 'NONE',  ( -73.89999999999997726, 0.2499224661714811724, 0.006225825468457807203 ) ) ;
#22632=CLOSED_SHELL ( 'NONE', ( #12426, #6787, #28011, #14434, #23758, #4547, #29954, #20763, #28779, #5357 ) ) ;
#22654=DIRECTION ( 'NONE',  ( 3.002035892788117459E-16, -0.9996898646859343485, -0.02490330187381124133 ) ) ;
#22703=CARTESIAN_POINT ( 'NONE',  ( -73.89999999999997726, -0.4498604391086729049, -0.01120648584321003519 ) ) ;
#22905=( NAMED_UNIT ( * ) PLANE_ANGLE_UNIT ( ) SI_UNIT ( $, .RADIAN. ) );
#22948=ORIENTED_EDGE ( 'NONE', *, *, #8203, .T. ) ;
#23038=VERTEX_POINT ( 'NONE', #22703 ) ;
#23123=DIRECTION ( 'NONE',  ( 3.002035892788116966E-16, -0.9996898646859343485, -0.02490330187381123786 ) ) ;
#23314=AXIS2_PLACEMENT_3D ( 'NONE', #27435, #13901, #29814 ) ;
#23351=AXIS2_PLACEMENT_3D ( 'NONE', #25447, #8661, #8516 ) ;
#23420=DIRECTION ( 'NONE',  ( 0.000000000000000000, -0.9996898646859343485, -0.02490330187381123786 ) ) ;
#23442=AXIS2_PLACEMENT_3D ( 'NONE', #20427, #8367, #22654 ) ;
#23568=EDGE_CURVE ( 'NONE', #3768, #8968, #28464, .T. ) ;
#23642=AXIS2_PLACEMENT_3D ( 'NONE', #14372, #14545, #12621 ) ;
#23736=CARTESIAN_POINT ( 'NONE',  ( -77.29999999999998295, -3.473832742311974792E-15, 5.302342620690189014E-15 ) ) ;
#23758=ADVANCED_FACE ( 'NONE', ( #28403 ), #14310, .T. ) ;
#23795=EDGE_LOOP ( 'NONE', ( #14942, #14901, #21932, #19399 ) ) ;
#23953=CARTESIAN_POINT ( 'NONE',  ( -73.89999999999997726, 0.4498604391086679644, 0.01120648584322002546 ) ) ;
#23999=EDGE_LOOP ( 'NONE', ( #31222, #21319 ) ) ;
#24162=CIRCLE ( 'NONE', #17096, 0.01000000000000001929 ) ;
#24413=AXIS2_PLACEMENT_3D ( 'NONE', #3860, #20673, #11141 ) ;
#24555=DIRECTION ( 'NONE',  ( 3.002035892788117952E-16, -0.9996898646859344595, -0.02490330187381124480 ) ) ;
#24624=ORIENTED_EDGE ( 'NONE', *, *, #23568, .T. ) ;
#24691=ORIENTED_EDGE ( 'NONE', *, *, #5748, .F. ) ;
#24699=MECHANICAL_DESIGN_GEOMETRIC_PRESENTATION_REPRESENTATION('',(#22192),#13569);
#24798=( NAMED_UNIT ( * ) SI_UNIT ( $, .STERADIAN. ) SOLID_ANGLE_UNIT ( ) );
#24942=( LENGTH_UNIT ( ) NAMED_UNIT ( * ) SI_UNIT ( .MILLI., .METRE. ) );
#25143=CARTESIAN_POINT ( 'NONE',  ( -73.89999999999997726, -0.2499224661714860851, -0.006225825468448203774 ) ) ;
#25164=ORIENTED_EDGE ( 'NONE', *, *, #26720, .F. ) ;
#25433=CARTESIAN_POINT ( 'NONE',  ( -77.29999999999998295, -3.473832742311974792E-15, 5.302342620690189014E-15 ) ) ;
#25447=CARTESIAN_POINT ( 'NONE',  ( -73.89999999999997726, -2.435524336289708093E-15, 4.607889071584891164E-15 ) ) ;
#25655=LINE ( 'NONE', #28192, #3299 ) ;
#25837=( LENGTH_UNIT ( ) NAMED_UNIT ( * ) SI_UNIT ( .MILLI., .METRE. ) );
#25908=ORIENTED_EDGE ( 'NONE', *, *, #29572, .T. ) ;
#25987=CARTESIAN_POINT ( 'NONE',  ( 0.000000000000000000, 0.000000000000000000, 0.000000000000000000 ) ) ;
#26062=VERTEX_POINT ( 'NONE', #23953 ) ;
#26157=AXIS2_PLACEMENT_3D ( 'NONE', #23736, #1695, #28319 ) ;
#26309=EDGE_LOOP ( 'NONE', ( #20714, #25164, #24624, #7011 ) ) ;
#26316=( NAMED_UNIT ( * ) PLANE_ANGLE_UNIT ( ) SI_UNIT ( $, .RADIAN. ) );
#26458=CYLINDRICAL_SURFACE ( 'NONE', #4898, 0.2500000000000000555 ) ;
#26589=DIRECTION ( 'NONE',  ( -1.000000000000000000, -3.053848253006669023E-16, 2.042510438544995415E-16 ) ) ;
#26709=AXIS2_PLACEMENT_3D ( 'NONE', #20094, #10255, #10108 ) ;
#26720=EDGE_CURVE ( 'NONE', #3768, #18823, #10993, .T. ) ;
#26757=ORIENTED_EDGE ( 'NONE', *, *, #29572, .F. ) ;
#26831=EDGE_CURVE ( 'NONE', #8781, #28086, #24162, .T. ) ;
#26874=DIRECTION ( 'NONE',  ( -2.117927888850090838E-16, 0.02490330187381123786, -0.9996898646859343485 ) ) ;
#26924=APPLICATION_CONTEXT ( 'automotive_design' ) ;
#27081=CARTESIAN_POINT ( 'NONE',  ( -44.49999999999997868, 0.2499224661714902207, 0.006225825468451445105 ) ) ;
#27237=DIRECTION ( 'NONE',  ( 1.000000000000000000, 3.053848253006669023E-16, -2.042510438544995415E-16 ) ) ;
#27379=DIRECTION ( 'NONE',  ( 1.000000000000000000, 3.053848253006669023E-16, -2.042510438544995415E-16 ) ) ;
#27435=CARTESIAN_POINT ( 'NONE',  ( -77.29999999999998295, -3.473832742311974792E-15, 5.302342620690189014E-15 ) ) ;
#27444=CARTESIAN_POINT ( 'NONE',  ( -77.29999999999998295, 0.4398635404618077005, 0.01095745282448230308 ) ) ;
#27480=CIRCLE ( 'NONE', #2211, 0.2500000000000000555 ) ;
#27804=VECTOR ( 'NONE', #29775, 1000.000000000000000 ) ;
#27821=ADVANCED_BREP_SHAPE_REPRESENTATION ( '', ( #15127, #9018 ), #18147 ) ;
#27855=DIRECTION ( 'NONE',  ( 0.000000000000000000, 0.9996898646859343485, 0.02490330187381123786 ) ) ;
#27884=DIRECTION ( 'NONE',  ( 1.000000000000000000, 3.053848253006669023E-16, -2.042510438544995415E-16 ) ) ;
#27985=APPLICATION_CONTEXT ( 'automotive_design' ) ;
#28011=ADVANCED_FACE ( 'NONE', ( #6304 ), #28631, .T. ) ;
#28047=ORIENTED_EDGE ( 'NONE', *, *, #21290, .T. ) ;
#28086=VERTEX_POINT ( 'NONE', #30513 ) ;
#28089=MECHANICAL_DESIGN_GEOMETRIC_PRESENTATION_REPRESENTATION('',(#21567),#296);
#28192=CARTESIAN_POINT ( 'NONE',  ( -77.29999999999998295, -0.4498604391086740151, -0.01120648584320970212 ) ) ;
#28319=DIRECTION ( 'NONE',  ( 0.000000000000000000, 0.9996898646859343485, 0.02490330187381123786 ) ) ;
#28403=FACE_OUTER_BOUND ( 'NONE', #26309, .T. ) ;
#28464=CIRCLE ( 'NONE', #4177, 0.01000000000000001929 ) ;
#28526=SURFACE_SIDE_STYLE ('',( #20942 ) ) ;
#28628=EDGE_CURVE ( 'NONE', #7995, #20300, #18621, .T. ) ;
#28631=CYLINDRICAL_SURFACE ( 'NONE', #26157, 0.4500000000000001221 ) ;
#28704=AXIS2_PLACEMENT_3D ( 'NONE', #13692, #13367, #4050 ) ;
#28742=DIRECTION ( 'NONE',  ( 0.000000000000000000, -0.9996898646859344595, -0.02490330187381123786 ) ) ;
#28779=ADVANCED_FACE ( 'NONE', ( #7096 ), #16279, .F. ) ;
#28784=SURFACE_STYLE_FILL_AREA ( #4700 ) ;
#28849=( NAMED_UNIT ( * ) SI_UNIT ( $, .STERADIAN. ) SOLID_ANGLE_UNIT ( ) );
#28907=CARTESIAN_POINT ( 'NONE',  ( -73.89999999999997726, -2.435524336289708093E-15, 4.607889071584891164E-15 ) ) ;
#28918=ORIENTED_EDGE ( 'NONE', *, *, #29349, .T. ) ;
#29227=ORIENTED_EDGE ( 'NONE', *, *, #18377, .F. ) ;
#29349=EDGE_CURVE ( 'NONE', #18823, #3768, #3372, .T. ) ;
#29544=EDGE_LOOP ( 'NONE', ( #9175, #18175, #18574, #337 ) ) ;
#29572=EDGE_CURVE ( 'NONE', #8781, #4844, #15500, .T. ) ;
#29775=DIRECTION ( 'NONE',  ( -1.000000000000000000, -3.053848253006669023E-16, 2.042510438544995415E-16 ) ) ;
#29783=PRODUCT_DEFINITION_SHAPE ( 'NONE', 'NONE',  #6040 ) ;
#29814=DIRECTION ( 'NONE',  ( 0.000000000000000000, -0.9996898646859343485, -0.02490330187381123786 ) ) ;
#29954=ADVANCED_FACE ( 'NONE', ( #18182, #1206 ), #20554, .T. ) ;
#30053=UNCERTAINTY_MEASURE_WITH_UNIT (LENGTH_MEASURE( 1.000000000000000082E-05 ), #16501, 'distance_accuracy_value', 'NONE');
#30061=FACE_OUTER_BOUND ( 'NONE', #18767, .T. ) ;
#30408=ORIENTED_EDGE ( 'NONE', *, *, #2445, .F. ) ;
#30513=CARTESIAN_POINT ( 'NONE',  ( -77.28999999999996362, -0.2499224661714871121, -0.006225825468447511619 ) ) ;
#30519=DIRECTION ( 'NONE',  ( 1.000000000000000000, 3.053848253006669023E-16, -2.042510438544995415E-16 ) ) ;
#30579=EDGE_CURVE ( 'NONE', #4844, #355, #1925, .T. ) ;
#30662=DIRECTION ( 'NONE',  ( -1.000000000000000000, -3.053848253006669023E-16, 2.042510438544995415E-16 ) ) ;
#30678=DIRECTION ( 'NONE',  ( -1.000000000000000000, -3.053848253006669023E-16, 2.042510438544995415E-16 ) ) ;
#30748=EDGE_LOOP ( 'NONE', ( #3235, #26757, #6413, #10677 ) ) ;
#30798=DIRECTION ( 'NONE',  ( 0.000000000000000000, -0.9996898646859343485, -0.02490330187381123786 ) ) ;
#30918=CIRCLE ( 'NONE', #23351, 0.4500000000000001221 ) ;
#30990=CARTESIAN_POINT ( 'NONE',  ( -44.49999999999997868, 6.542789527549899840E-15, -1.397091617737396343E-15 ) ) ;
#31191=CARTESIAN_POINT ( 'NONE',  ( -44.49999999999997868, -0.2499224661714770923, -0.006225825468454208519 ) ) ;
#31203=ORIENTED_EDGE ( 'NONE', *, *, #8668, .T. ) ;
#31222=ORIENTED_EDGE ( 'NONE', *, *, #28628, .F. ) ;
#31244=AXIS2_PLACEMENT_3D ( 'NONE', #19657, #317, #14407 ) ;
ENDSEC;
END-ISO-10303-21;
